ISO-10303-21;
HEADER;
FILE_DESCRIPTION (('STEP AP214'),
    '1' );
FILE_NAME ('dead centre.step',
    '2026-10-26T19:46:16',
    ( '' ),
    ( '' ),
    'SwSTEP 2.0',
    'SolidWorks 2025',
    '' );
FILE_SCHEMA (( 'AUTOMOTIVE_DESIGN' ));
ENDSEC;

DATA;
#127=CONICAL_SURFACE ( 'NONE', #43492, 10.99999999999998934, 0.5235987755982931535 ) ;
#243=CARTESIAN_POINT ( 'NONE',  ( 0.000000000000000000, 19.05255888325788050, 10.99999999999998934 ) ) ;
#300=VERTEX_POINT ( 'NONE', #243 ) ;
#544=ORIENTED_EDGE ( 'NONE', *, *, #25083, .T. ) ;
#845=UNCERTAINTY_MEASURE_WITH_UNIT (LENGTH_MEASURE( 1.000000000000000082E-05 ), #3126, 'distance_accuracy_value', 'NONE');
#1082=ADVANCED_FACE ( 'NONE', ( #52525 ), #41571, .T. ) ;
#1289=DIRECTION ( 'NONE',  ( 0.000000000000000000, 0.000000000000000000, 1.000000000000000000 ) ) ;
#1429=EDGE_CURVE ( 'NONE', #22621, #11774, #13546, .T. ) ;
#1533=AXIS2_PLACEMENT_3D ( 'NONE', #55079, #71286, #32442 ) ;
#2150=SHAPE_REPRESENTATION ( 'dead centre', ( #57354 ), #21241 ) ;
#2405=EDGE_CURVE ( 'NONE', #39639, #38422, #55771, .T. ) ;
#3107=AXIS2_PLACEMENT_3D ( 'NONE', #67726, #50733, #10748 ) ;
#3126=( LENGTH_UNIT ( ) NAMED_UNIT ( * ) SI_UNIT ( .MILLI., .METRE. ) );
#3386=DIRECTION ( 'NONE',  ( 0.000000000000000000, 0.000000000000000000, 1.000000000000000000 ) ) ;
#4855=EDGE_CURVE ( 'NONE', #300, #27460, #9676, .T. ) ;
#5438=VECTOR ( 'NONE', #61645, 1000.000000000000000 ) ;
#5718=DIRECTION ( 'NONE',  ( 0.000000000000000000, 0.8660254037844414832, 0.4999999999999950595 ) ) ;
#5767=ADVANCED_FACE ( 'NONE', ( #59150 ), #10952, .T. ) ;
#7405=DIRECTION ( 'NONE',  ( 0.000000000000000000, 0.000000000000000000, 1.000000000000000000 ) ) ;
#7459=CARTESIAN_POINT ( 'NONE',  ( 0.000000000000000000, 101.0525588832578734, 0.000000000000000000 ) ) ;
#7645=DIRECTION ( 'NONE',  ( -0.000000000000000000, 1.000000000000000000, -0.000000000000000000 ) ) ;
#8373=CARTESIAN_POINT ( 'NONE',  ( 0.000000000000000000, 101.0525588832578734, 0.000000000000000000 ) ) ;
#8688=CARTESIAN_POINT ( 'NONE',  ( 1.347111479062087024E-15, 101.0525588832578734, -10.99999999999998934 ) ) ;
#8960=EDGE_LOOP ( 'NONE', ( #15397, #72908, #73570, #57830 ) ) ;
#9154=( NAMED_UNIT ( * ) PLANE_ANGLE_UNIT ( ) SI_UNIT ( $, .RADIAN. ) );
#9480=( NAMED_UNIT ( * ) PLANE_ANGLE_UNIT ( ) SI_UNIT ( $, .RADIAN. ) );
#9676=LINE ( 'NONE', #32697, #33803 ) ;
#10357=ORIENTED_EDGE ( 'NONE', *, *, #50193, .F. ) ;
#10461=AXIS2_PLACEMENT_3D ( 'NONE', #28286, #46004, #62605 ) ;
#10748=DIRECTION ( 'NONE',  ( 0.000000000000000000, 0.000000000000000000, 1.000000000000000000 ) ) ;
#10867=CIRCLE ( 'NONE', #49424, 10.19999999999999396 ) ;
#10952=CONICAL_SURFACE ( 'NONE', #67550, 7.949999999999993960, 0.04496966185232758456 ) ;
#11042=STYLED_ITEM('',(#74685),#16907);
#11422=DIRECTION ( 'NONE',  ( 0.000000000000000000, 0.000000000000000000, 1.000000000000000000 ) ) ;
#11774=VERTEX_POINT ( 'NONE', #50017 ) ;
#11996=ORIENTED_EDGE ( 'NONE', *, *, #73976, .F. ) ;
#12362=ORIENTED_EDGE ( 'NONE', *, *, #4855, .F. ) ;
#13035=DIRECTION ( 'NONE',  ( -0.000000000000000000, 1.000000000000000000, -0.000000000000000000 ) ) ;
#13546=CIRCLE ( 'NONE', #1533, 7.949999999999993960 ) ;
#13603=ORIENTED_EDGE ( 'NONE', *, *, #24311, .T. ) ;
#13892=VECTOR ( 'NONE', #32461, 1000.000000000000000 ) ;
#13965=EDGE_LOOP ( 'NONE', ( #50723, #544, #10357 ) ) ;
#14588=CARTESIAN_POINT ( 'NONE',  ( 0.000000000000000000, 51.05255888325788050, 0.000000000000000000 ) ) ;
#14823=ADVANCED_FACE ( 'NONE', ( #67137 ), #127, .T. ) ;
#14844=ORIENTED_EDGE ( 'NONE', *, *, #31146, .T. ) ;
#15102=AXIS2_PLACEMENT_3D ( 'NONE', #65484, #71499, #43207 ) ;
#15172=ORIENTED_EDGE ( 'NONE', *, *, #26239, .F. ) ;
#15397=ORIENTED_EDGE ( 'NONE', *, *, #72663, .F. ) ;
#15891=CARTESIAN_POINT ( 'NONE',  ( 9.735942053221449011E-16, 101.0525588832578734, 7.949999999999993960 ) ) ;
#15977=LINE ( 'NONE', #21640, #5438 ) ;
#16907=MANIFOLD_SOLID_BREP ( 'Revolve1', #23782 ) ;
#16959=DIRECTION ( 'NONE',  ( 0.000000000000000000, 0.000000000000000000, 1.000000000000000000 ) ) ;
#17067=DIRECTION ( 'NONE',  ( -0.000000000000000000, 1.000000000000000000, -0.000000000000000000 ) ) ;
#17216=EDGE_CURVE ( 'NONE', #21786, #27460, #33897, .T. ) ;
#17809=VECTOR ( 'NONE', #39216, 1000.000000000000000 ) ;
#19434=EDGE_CURVE ( 'NONE', #22621, #38422, #67594, .T. ) ;
#19676=APPLICATION_CONTEXT ( 'automotive_design' ) ;
#19735=ORIENTED_EDGE ( 'NONE', *, *, #67147, .F. ) ;
#19816=DIRECTION ( 'NONE',  ( -0.000000000000000000, 1.000000000000000000, -0.000000000000000000 ) ) ;
#20024=( NAMED_UNIT ( * ) SI_UNIT ( $, .STERADIAN. ) SOLID_ANGLE_UNIT ( ) );
#21241=( GEOMETRIC_REPRESENTATION_CONTEXT ( 3 ) GLOBAL_UNCERTAINTY_ASSIGNED_CONTEXT ( ( #47142 ) ) GLOBAL_UNIT_ASSIGNED_CONTEXT ( ( #67191, #9480, #20024 ) ) REPRESENTATION_CONTEXT ( 'NONE', 'WORKASPACE' ) );
#21640=CARTESIAN_POINT ( 'NONE',  ( 0.000000000000000000, 101.0525588832578734, -7.949999999999993960 ) ) ;
#21734=AXIS2_PLACEMENT_3D ( 'NONE', #29577, #23538, #47284 ) ;
#21786=VERTEX_POINT ( 'NONE', #39269 ) ;
#22621=VERTEX_POINT ( 'NONE', #64328 ) ;
#23006=ORIENTED_EDGE ( 'NONE', *, *, #25083, .F. ) ;
#23538=DIRECTION ( 'NONE',  ( -0.000000000000000000, 1.000000000000000000, -0.000000000000000000 ) ) ;
#23694=DIRECTION ( 'NONE',  ( 0.000000000000000000, -1.000000000000000000, 0.000000000000000000 ) ) ;
#23782=CLOSED_SHELL ( 'NONE', ( #14823, #31453, #5767, #37438, #35107, #73617, #1082, #44738 ) ) ;
#24056=CARTESIAN_POINT ( 'NONE',  ( 0.000000000000000000, 101.0525588832578734, 0.000000000000000000 ) ) ;
#24311=EDGE_CURVE ( 'NONE', #58992, #300, #39673, .T. ) ;
#24404=AXIS2_PLACEMENT_3D ( 'NONE', #47644, #43378, #1289 ) ;
#25083=EDGE_CURVE ( 'NONE', #58992, #39682, #33949, .T. ) ;
#25369=( NAMED_UNIT ( * ) SI_UNIT ( $, .STERADIAN. ) SOLID_ANGLE_UNIT ( ) );
#25410=ORIENTED_EDGE ( 'NONE', *, *, #32745, .T. ) ;
#25582=CIRCLE ( 'NONE', #69023, 10.99999999999998934 ) ;
#25591=ORIENTED_EDGE ( 'NONE', *, *, #19434, .F. ) ;
#26016=LINE ( 'NONE', #8688, #13892 ) ;
#26239=EDGE_CURVE ( 'NONE', #39682, #300, #36023, .T. ) ;
#27460=VERTEX_POINT ( 'NONE', #44951 ) ;
#28286=CARTESIAN_POINT ( 'NONE',  ( 0.000000000000000000, 101.0525588832578734, 7.949999999999993960 ) ) ;
#28628=VECTOR ( 'NONE', #5718, 1000.000000000000000 ) ;
#28983=FACE_OUTER_BOUND ( 'NONE', #62617, .T. ) ;
#29577=CARTESIAN_POINT ( 'NONE',  ( 0.000000000000000000, 101.0525588832578734, 0.000000000000000000 ) ) ;
#30655=ORIENTED_EDGE ( 'NONE', *, *, #2405, .F. ) ;
#31146=EDGE_CURVE ( 'NONE', #38422, #39639, #10867, .T. ) ;
#31453=ADVANCED_FACE ( 'NONE', ( #58269 ), #41268, .T. ) ;
#32442=DIRECTION ( 'NONE',  ( 0.000000000000000000, 0.000000000000000000, 1.000000000000000000 ) ) ;
#32461=DIRECTION ( 'NONE',  ( -0.000000000000000000, 1.000000000000000000, -0.000000000000000000 ) ) ;
#32624=ORIENTED_EDGE ( 'NONE', *, *, #1429, .F. ) ;
#32697=CARTESIAN_POINT ( 'NONE',  ( 0.000000000000000000, 101.0525588832578734, 10.99999999999998934 ) ) ;
#32745=EDGE_CURVE ( 'NONE', #11774, #22621, #43117, .T. ) ;
#33803=VECTOR ( 'NONE', #38725, 1000.000000000000000 ) ;
#33897=CIRCLE ( 'NONE', #67644, 10.99999999999999112 ) ;
#33949=LINE ( 'NONE', #73536, #17809 ) ;
#34459=DIRECTION ( 'NONE',  ( 1.000000000000000000, 0.000000000000000000, 0.000000000000000000 ) ) ;
#34750=CARTESIAN_POINT ( 'NONE',  ( 0.000000000000000000, 0.000000000000000000, 0.000000000000000000 ) ) ;
#35107=ADVANCED_FACE ( 'NONE', ( #28983 ), #54066, .T. ) ;
#35641=CIRCLE ( 'NONE', #3107, 10.99999999999999112 ) ;
#35702=FACE_OUTER_BOUND ( 'NONE', #69366, .T. ) ;
#36023=CIRCLE ( 'NONE', #46846, 10.99999999999998934 ) ;
#36439=CARTESIAN_POINT ( 'NONE',  ( 0.000000000000000000, 19.05255888325788050, 0.000000000000000000 ) ) ;
#36475=ORIENTED_EDGE ( 'NONE', *, *, #50193, .T. ) ;
#36687=DIRECTION ( 'NONE',  ( 0.000000000000000000, 0.000000000000000000, 1.000000000000000000 ) ) ;
#36868=DIRECTION ( 'NONE',  ( 0.000000000000000000, 0.000000000000000000, -1.000000000000000000 ) ) ;
#37367=DIRECTION ( 'NONE',  ( -0.000000000000000000, 1.000000000000000000, -0.000000000000000000 ) ) ;
#37378=EDGE_LOOP ( 'NONE', ( #25410, #56940 ) ) ;
#37438=ADVANCED_FACE ( 'NONE', ( #45263 ), #68275, .T. ) ;
#38422=VERTEX_POINT ( 'NONE', #63732 ) ;
#38725=DIRECTION ( 'NONE',  ( -0.000000000000000000, 1.000000000000000000, -0.000000000000000000 ) ) ;
#38922=DIRECTION ( 'NONE',  ( 5.505339259226019480E-18, -0.9989890351440378069, 0.04495450658148170825 ) ) ;
#39216=DIRECTION ( 'NONE',  ( 6.123233995736705639E-17, 0.8660254037844414832, -0.4999999999999950595 ) ) ;
#39269=CARTESIAN_POINT ( 'NONE',  ( 1.347111479062087419E-15, 51.05255888325788050, -10.99999999999999112 ) ) ;
#39550=PRODUCT_CONTEXT ( 'NONE', #19676, 'mechanical' ) ;
#39639=VERTEX_POINT ( 'NONE', #50763 ) ;
#39673=LINE ( 'NONE', #45697, #28628 ) ;
#39682=VERTEX_POINT ( 'NONE', #73778 ) ;
#39982=CARTESIAN_POINT ( 'NONE',  ( 0.000000000000000000, 19.05255888325788050, 0.000000000000000000 ) ) ;
#41268=CYLINDRICAL_SURFACE ( 'NONE', #21734, 10.99999999999998934 ) ;
#41571=CYLINDRICAL_SURFACE ( 'NONE', #43694, 10.99999999999998934 ) ;
#41931=AXIS2_PLACEMENT_3D ( 'NONE', #8373, #7645, #36687 ) ;
#42459=CARTESIAN_POINT ( 'NONE',  ( 0.000000000000000000, 19.05255888325788050, 0.000000000000000000 ) ) ;
#42467=FACE_BOUND ( 'NONE', #56329, .T. ) ;
#43013=ORIENTED_EDGE ( 'NONE', *, *, #31146, .F. ) ;
#43117=CIRCLE ( 'NONE', #41931, 7.949999999999993960 ) ;
#43207=DIRECTION ( 'NONE',  ( 0.000000000000000000, 0.000000000000000000, 1.000000000000000000 ) ) ;
#43378=DIRECTION ( 'NONE',  ( -0.000000000000000000, 1.000000000000000000, -0.000000000000000000 ) ) ;
#43492=AXIS2_PLACEMENT_3D ( 'NONE', #50891, #73530, #3386 ) ;
#43694=AXIS2_PLACEMENT_3D ( 'NONE', #68755, #17067, #63462 ) ;
#44193=PRODUCT_DEFINITION_FORMATION_WITH_SPECIFIED_SOURCE ( 'ANY', '', #68009, .NOT_KNOWN. ) ;
#44738=ADVANCED_FACE ( 'NONE', ( #35702 ), #54477, .T. ) ;
#44951=CARTESIAN_POINT ( 'NONE',  ( 0.000000000000000000, 51.05255888325788050, 10.99999999999999112 ) ) ;
#45263=FACE_OUTER_BOUND ( 'NONE', #37378, .T. ) ;
#45697=CARTESIAN_POINT ( 'NONE',  ( 0.000000000000000000, 19.05255888325788050, 10.99999999999998934 ) ) ;
#46004=DIRECTION ( 'NONE',  ( -0.000000000000000000, 1.000000000000000000, 0.000000000000000000 ) ) ;
#46492=ORIENTED_EDGE ( 'NONE', *, *, #73976, .T. ) ;
#46846=AXIS2_PLACEMENT_3D ( 'NONE', #39982, #62989, #16959 ) ;
#46963=ORIENTED_EDGE ( 'NONE', *, *, #72663, .T. ) ;
#47005=DIRECTION ( 'NONE',  ( 0.000000000000000000, 0.000000000000000000, 1.000000000000000000 ) ) ;
#47142=UNCERTAINTY_MEASURE_WITH_UNIT (LENGTH_MEASURE( 1.000000000000000082E-05 ), #67191, 'distance_accuracy_value', 'NONE');
#47284=DIRECTION ( 'NONE',  ( 0.000000000000000000, 0.000000000000000000, 1.000000000000000000 ) ) ;
#47644=CARTESIAN_POINT ( 'NONE',  ( 0.000000000000000000, 51.05255888325788050, 0.000000000000000000 ) ) ;
#47923=ORIENTED_EDGE ( 'NONE', *, *, #19434, .T. ) ;
#48921=DIRECTION ( 'NONE',  ( -0.000000000000000000, 1.000000000000000000, -0.000000000000000000 ) ) ;
#49424=AXIS2_PLACEMENT_3D ( 'NONE', #14588, #48921, #71934 ) ;
#49551=ORIENTED_EDGE ( 'NONE', *, *, #67147, .T. ) ;
#49590=VECTOR ( 'NONE', #38922, 1000.000000000000000 ) ;
#50017=CARTESIAN_POINT ( 'NONE',  ( 0.000000000000000000, 101.0525588832578734, -7.949999999999993960 ) ) ;
#50193=EDGE_CURVE ( 'NONE', #300, #39682, #25582, .T. ) ;
#50528=PRODUCT_DEFINITION_SHAPE ( 'NONE', 'NONE',  #51928 ) ;
#50723=ORIENTED_EDGE ( 'NONE', *, *, #24311, .F. ) ;
#50733=DIRECTION ( 'NONE',  ( -0.000000000000000000, 1.000000000000000000, -0.000000000000000000 ) ) ;
#50760=MECHANICAL_DESIGN_GEOMETRIC_PRESENTATION_REPRESENTATION('',(#11042),#53196);
#50763=CARTESIAN_POINT ( 'NONE',  ( 0.000000000000000000, 51.05255888325788050, -10.19999999999999396 ) ) ;
#50891=CARTESIAN_POINT ( 'NONE',  ( 0.000000000000000000, 19.05255888325788050, 0.000000000000000000 ) ) ;
#51100=APPLICATION_CONTEXT ( 'automotive_design' ) ;
#51928=PRODUCT_DEFINITION ( 'UNKNOWN', '', #44193, #56892 ) ;
#52525=FACE_OUTER_BOUND ( 'NONE', #8960, .T. ) ;
#53196=( GEOMETRIC_REPRESENTATION_CONTEXT ( 3 ) GLOBAL_UNCERTAINTY_ASSIGNED_CONTEXT ( ( #845 ) ) GLOBAL_UNIT_ASSIGNED_CONTEXT ( ( #3126, #9154, #25369 ) ) REPRESENTATION_CONTEXT ( 'NONE', 'WORKASPACE' ) );
#53290=AXIS2_PLACEMENT_3D ( 'NONE', #36439, #13035, #47005 ) ;
#53440=PLANE ( 'NONE',  #15102 ) ;
#53737=ORIENTED_EDGE ( 'NONE', *, *, #32745, .F. ) ;
#54066=CONICAL_SURFACE ( 'NONE', #64874, 7.949999999999993960, 0.04496966185232758456 ) ;
#54477=CONICAL_SURFACE ( 'NONE', #53290, 10.99999999999998934, 0.5235987755982931535 ) ;
#55079=CARTESIAN_POINT ( 'NONE',  ( 0.000000000000000000, 101.0525588832578734, 0.000000000000000000 ) ) ;
#55158=ADVANCED_BREP_SHAPE_REPRESENTATION ( '', ( #16907, #57354 ), #21241 ) ;
#55771=CIRCLE ( 'NONE', #24404, 10.19999999999999396 ) ;
#56329=EDGE_LOOP ( 'NONE', ( #30655, #43013 ) ) ;
#56892=PRODUCT_DEFINITION_CONTEXT ( 'detailed design', #51100, 'design' ) ;
#56940=ORIENTED_EDGE ( 'NONE', *, *, #1429, .T. ) ;
#57354=AXIS2_PLACEMENT_3D ( 'NONE', #63097, #11422, #34459 ) ;
#57830=ORIENTED_EDGE ( 'NONE', *, *, #17216, .F. ) ;
#58269=FACE_OUTER_BOUND ( 'NONE', #68026, .T. ) ;
#58417=DIRECTION ( 'NONE',  ( 0.000000000000000000, 0.000000000000000000, -1.000000000000000000 ) ) ;
#58992=VERTEX_POINT ( 'NONE', #34750 ) ;
#59150=FACE_OUTER_BOUND ( 'NONE', #64607, .T. ) ;
#61645=DIRECTION ( 'NONE',  ( 0.000000000000000000, -0.9989890351440378069, -0.04495450658148170825 ) ) ;
#62605=DIRECTION ( 'NONE',  ( 0.000000000000000000, 0.000000000000000000, 1.000000000000000000 ) ) ;
#62617=EDGE_LOOP ( 'NONE', ( #25591, #53737, #49551, #71618 ) ) ;
#62989=DIRECTION ( 'NONE',  ( -0.000000000000000000, 1.000000000000000000, -0.000000000000000000 ) ) ;
#63097=CARTESIAN_POINT ( 'NONE',  ( 0.000000000000000000, 0.000000000000000000, 0.000000000000000000 ) ) ;
#63462=DIRECTION ( 'NONE',  ( 0.000000000000000000, 0.000000000000000000, 1.000000000000000000 ) ) ;
#63732=CARTESIAN_POINT ( 'NONE',  ( 1.249139735130299379E-15, 51.05255888325788050, 10.19999999999999396 ) ) ;
#64190=CARTESIAN_POINT ( 'NONE',  ( 0.000000000000000000, 51.05255888325788050, 0.000000000000000000 ) ) ;
#64328=CARTESIAN_POINT ( 'NONE',  ( 1.111366970226222140E-15, 101.0525588832578734, 7.949999999999993960 ) ) ;
#64607=EDGE_LOOP ( 'NONE', ( #32624, #47923, #14844, #19735 ) ) ;
#64874=AXIS2_PLACEMENT_3D ( 'NONE', #24056, #23694, #58417 ) ;
#65285=DIRECTION ( 'NONE',  ( 0.000000000000000000, 0.000000000000000000, 1.000000000000000000 ) ) ;
#65484=CARTESIAN_POINT ( 'NONE',  ( 0.000000000000000000, 51.05255888325788050, 10.99999999999999112 ) ) ;
#66429=SHAPE_REPRESENTATION_RELATIONSHIP ( 'NONE' , 'NONE' ,  #2150, #55158 ) ;
#67137=FACE_OUTER_BOUND ( 'NONE', #13965, .T. ) ;
#67147=EDGE_CURVE ( 'NONE', #11774, #39639, #15977, .T. ) ;
#67191=( LENGTH_UNIT ( ) NAMED_UNIT ( * ) SI_UNIT ( .MILLI., .METRE. ) );
#67550=AXIS2_PLACEMENT_3D ( 'NONE', #7459, #71924, #36868 ) ;
#67594=LINE ( 'NONE', #15891, #49590 ) ;
#67644=AXIS2_PLACEMENT_3D ( 'NONE', #64190, #37367, #65285 ) ;
#67726=CARTESIAN_POINT ( 'NONE',  ( 0.000000000000000000, 51.05255888325788050, 0.000000000000000000 ) ) ;
#68009=PRODUCT ( 'dead centre', 'dead centre', '', ( #39550 ) ) ;
#68026=EDGE_LOOP ( 'NONE', ( #36475, #46963, #11996, #12362 ) ) ;
#68275=PLANE ( 'NONE',  #10461 ) ;
#68585=SHAPE_DEFINITION_REPRESENTATION ( #50528, #2150 ) ;
#68755=CARTESIAN_POINT ( 'NONE',  ( 0.000000000000000000, 101.0525588832578734, 0.000000000000000000 ) ) ;
#69023=AXIS2_PLACEMENT_3D ( 'NONE', #42459, #19816, #7405 ) ;
#69366=EDGE_LOOP ( 'NONE', ( #23006, #13603, #15172 ) ) ;
#70589=ORIENTED_EDGE ( 'NONE', *, *, #17216, .T. ) ;
#70841=EDGE_LOOP ( 'NONE', ( #46492, #70589 ) ) ;
#71286=DIRECTION ( 'NONE',  ( -0.000000000000000000, 1.000000000000000000, -0.000000000000000000 ) ) ;
#71499=DIRECTION ( 'NONE',  ( -0.000000000000000000, 1.000000000000000000, 0.000000000000000000 ) ) ;
#71618=ORIENTED_EDGE ( 'NONE', *, *, #2405, .T. ) ;
#71874=FACE_OUTER_BOUND ( 'NONE', #70841, .T. ) ;
#71924=DIRECTION ( 'NONE',  ( 0.000000000000000000, -1.000000000000000000, 0.000000000000000000 ) ) ;
#71934=DIRECTION ( 'NONE',  ( 0.000000000000000000, 0.000000000000000000, 1.000000000000000000 ) ) ;
#72663=EDGE_CURVE ( 'NONE', #39682, #21786, #26016, .T. ) ;
#72908=ORIENTED_EDGE ( 'NONE', *, *, #26239, .T. ) ;
#73530=DIRECTION ( 'NONE',  ( -0.000000000000000000, 1.000000000000000000, -0.000000000000000000 ) ) ;
#73536=CARTESIAN_POINT ( 'NONE',  ( 1.347111479062087024E-15, 19.05255888325788050, -10.99999999999998934 ) ) ;
#73570=ORIENTED_EDGE ( 'NONE', *, *, #4855, .T. ) ;
#73617=ADVANCED_FACE ( 'NONE', ( #71874, #42467 ), #53440, .T. ) ;
#73778=CARTESIAN_POINT ( 'NONE',  ( 1.347111479062087024E-15, 19.05255888325788050, -10.99999999999998934 ) ) ;
#73976=EDGE_CURVE ( 'NONE', #27460, #21786, #35641, .T. ) ;
#74679=COLOUR_RGB('Light Blue',0.38,0.62,0.78);
#74680=FILL_AREA_STYLE_COLOUR('',#74679);
#74681=FILL_AREA_STYLE('',(#74680));
#74682=SURFACE_STYLE_FILL_AREA(#74681);
#74683=SURFACE_SIDE_STYLE('',(#74682));
#74684=SURFACE_STYLE_USAGE(.BOTH.,#74683);
#74685=PRESENTATION_STYLE_ASSIGNMENT((#74684));
ENDSEC;
END-ISO-10303-21;
